ISO-10303-21;
HEADER;
/* Generated by software containing ST-Developer
 * from STEP Tools, Inc. (www.steptools.com) 
 */

FILE_DESCRIPTION(
/* description */ (''),
/* implementation_level */ '2;1');

FILE_NAME(
/* name */ 'Front_Mount.step',
/* time_stamp */ '2026-10-23T22:30:33+06:00',
/* author */ (''),
/* organization */ (''),
/* preprocessor_version */ 'ST-DEVELOPER v20.2',
/* originating_system */ 'Autodesk Translation Framework v15.15.0.0',
/* authorisation */ '');

FILE_SCHEMA (('AUTOMOTIVE_DESIGN { 1 0 10303 214 3 1 1 }'));
ENDSEC;

DATA;
#10=MECHANICAL_DESIGN_GEOMETRIC_PRESENTATION_REPRESENTATION('',(#240),#10131);
#220=SHAPE_REPRESENTATION_RELATIONSHIP('SRR','None',#10174,#230);
#230=ADVANCED_BREP_SHAPE_REPRESENTATION('',(#250),#10126);
#240=STYLED_ITEM('',(#10261),#250);
#250=MANIFOLD_SOLID_BREP('Front_Mount',#5884);
#301=FACE_BOUND('',#1040,.T.);
#302=FACE_BOUND('',#1043,.T.);
#303=FACE_BOUND('',#1044,.T.);
#304=FACE_BOUND('',#1047,.T.);
#398=PLANE('',#6316);
#399=PLANE('',#6317);
#400=PLANE('',#6318);
#401=PLANE('',#6319);
#402=PLANE('',#6320);
#403=PLANE('',#6321);
#404=PLANE('',#6322);
#405=PLANE('',#6323);
#406=PLANE('',#6324);
#407=PLANE('',#6325);
#640=FACE_OUTER_BOUND('',#1035,.T.);
#641=FACE_OUTER_BOUND('',#1036,.T.);
#642=FACE_OUTER_BOUND('',#1037,.T.);
#643=FACE_OUTER_BOUND('',#1038,.T.);
#644=FACE_OUTER_BOUND('',#1039,.T.);
#645=FACE_OUTER_BOUND('',#1041,.T.);
#646=FACE_OUTER_BOUND('',#1042,.T.);
#647=FACE_OUTER_BOUND('',#1045,.T.);
#648=FACE_OUTER_BOUND('',#1046,.T.);
#649=FACE_OUTER_BOUND('',#1048,.T.);
#650=FACE_OUTER_BOUND('',#1049,.T.);
#651=FACE_OUTER_BOUND('',#1050,.T.);
#1035=EDGE_LOOP('',(#4534,#4535,#4536,#4537));
#1036=EDGE_LOOP('',(#4538,#4539,#4540,#4541));
#1037=EDGE_LOOP('',(#4542,#4543,#4544,#4545,#4546,#4547,#4548,#4549));
#1038=EDGE_LOOP('',(#4550,#4551,#4552,#4553));
#1039=EDGE_LOOP('',(#4554,#4555,#4556,#4557));
#1040=EDGE_LOOP('',(#4558));
#1041=EDGE_LOOP('',(#4559,#4560,#4561,#4562));
#1042=EDGE_LOOP('',(#4563,#4564,#4565,#4566));
#1043=EDGE_LOOP('',(#4567));
#1044=EDGE_LOOP('',(#4568));
#1045=EDGE_LOOP('',(#4569,#4570,#4571,#4572));
#1046=EDGE_LOOP('',(#4573,#4574,#4575,#4576));
#1047=EDGE_LOOP('',(#4577));
#1048=EDGE_LOOP('',(#4578,#4579,#4580,#4581));
#1049=EDGE_LOOP('',(#4582,#4583,#4584,#4585));
#1050=EDGE_LOOP('',(#4586,#4587,#4588,#4589,#4590,#4591,#4592,#4593));
#1509=LINE('',#9291,#2059);
#1510=LINE('',#9297,#2060);
#1511=LINE('',#9302,#2061);
#1512=LINE('',#9304,#2062);
#1513=LINE('',#9306,#2063);
#1514=LINE('',#9308,#2064);
#1515=LINE('',#9310,#2065);
#1516=LINE('',#9312,#2066);
#1517=LINE('',#9314,#2067);
#1518=LINE('',#9315,#2068);
#1519=LINE('',#9318,#2069);
#1520=LINE('',#9320,#2070);
#1521=LINE('',#9321,#2071);
#1522=LINE('',#9324,#2072);
#1523=LINE('',#9325,#2073);
#1524=LINE('',#9328,#2074);
#1525=LINE('',#9329,#2075);
#1526=LINE('',#9332,#2076);
#1527=LINE('',#9333,#2077);
#1528=LINE('',#9336,#2078);
#1529=LINE('',#9337,#2079);
#1530=LINE('',#9340,#2080);
#1531=LINE('',#9341,#2081);
#1532=LINE('',#9344,#2082);
#1533=LINE('',#9345,#2083);
#1534=LINE('',#9347,#2084);
#2059=VECTOR('',#7521,3.00000000000001);
#2060=VECTOR('',#7528,3.);
#2061=VECTOR('',#7533,10.);
#2062=VECTOR('',#7534,10.);
#2063=VECTOR('',#7535,10.);
#2064=VECTOR('',#7536,10.);
#2065=VECTOR('',#7537,10.);
#2066=VECTOR('',#7538,10.);
#2067=VECTOR('',#7539,10.);
#2068=VECTOR('',#7540,10.);
#2069=VECTOR('',#7543,10.);
#2070=VECTOR('',#7544,10.);
#2071=VECTOR('',#7545,10.);
#2072=VECTOR('',#7548,10.);
#2073=VECTOR('',#7549,10.);
#2074=VECTOR('',#7552,10.);
#2075=VECTOR('',#7553,10.);
#2076=VECTOR('',#7556,10.);
#2077=VECTOR('',#7557,10.);
#2078=VECTOR('',#7560,10.);
#2079=VECTOR('',#7561,10.);
#2080=VECTOR('',#7564,10.);
#2081=VECTOR('',#7565,10.);
#2082=VECTOR('',#7568,10.);
#2083=VECTOR('',#7569,10.);
#2084=VECTOR('',#7572,10.);
#2400=CIRCLE('',#6311,3.00000000000001);
#2401=CIRCLE('',#6312,3.00000000000001);
#2402=CIRCLE('',#6314,3.);
#2403=CIRCLE('',#6315,3.);
#2676=VERTEX_POINT('',#9288);
#2677=VERTEX_POINT('',#9290);
#2678=VERTEX_POINT('',#9294);
#2679=VERTEX_POINT('',#9296);
#2680=VERTEX_POINT('',#9300);
#2681=VERTEX_POINT('',#9301);
#2682=VERTEX_POINT('',#9303);
#2683=VERTEX_POINT('',#9305);
#2684=VERTEX_POINT('',#9307);
#2685=VERTEX_POINT('',#9309);
#2686=VERTEX_POINT('',#9311);
#2687=VERTEX_POINT('',#9313);
#2688=VERTEX_POINT('',#9317);
#2689=VERTEX_POINT('',#9319);
#2690=VERTEX_POINT('',#9323);
#2691=VERTEX_POINT('',#9327);
#2692=VERTEX_POINT('',#9331);
#2693=VERTEX_POINT('',#9335);
#2694=VERTEX_POINT('',#9339);
#2695=VERTEX_POINT('',#9343);
#3319=EDGE_CURVE('',#2676,#2676,#2400,.T.);
#3320=EDGE_CURVE('',#2676,#2677,#1509,.T.);
#3321=EDGE_CURVE('',#2677,#2677,#2401,.T.);
#3322=EDGE_CURVE('',#2678,#2678,#2402,.T.);
#3323=EDGE_CURVE('',#2678,#2679,#1510,.T.);
#3324=EDGE_CURVE('',#2679,#2679,#2403,.T.);
#3325=EDGE_CURVE('',#2680,#2681,#1511,.T.);
#3326=EDGE_CURVE('',#2681,#2682,#1512,.T.);
#3327=EDGE_CURVE('',#2682,#2683,#1513,.T.);
#3328=EDGE_CURVE('',#2683,#2684,#1514,.T.);
#3329=EDGE_CURVE('',#2684,#2685,#1515,.T.);
#3330=EDGE_CURVE('',#2685,#2686,#1516,.T.);
#3331=EDGE_CURVE('',#2686,#2687,#1517,.T.);
#3332=EDGE_CURVE('',#2687,#2680,#1518,.T.);
#3333=EDGE_CURVE('',#2681,#2688,#1519,.T.);
#3334=EDGE_CURVE('',#2689,#2688,#1520,.T.);
#3335=EDGE_CURVE('',#2682,#2689,#1521,.T.);
#3336=EDGE_CURVE('',#2690,#2689,#1522,.T.);
#3337=EDGE_CURVE('',#2683,#2690,#1523,.T.);
#3338=EDGE_CURVE('',#2691,#2690,#1524,.T.);
#3339=EDGE_CURVE('',#2684,#2691,#1525,.T.);
#3340=EDGE_CURVE('',#2692,#2691,#1526,.T.);
#3341=EDGE_CURVE('',#2685,#2692,#1527,.T.);
#3342=EDGE_CURVE('',#2693,#2692,#1528,.T.);
#3343=EDGE_CURVE('',#2686,#2693,#1529,.T.);
#3344=EDGE_CURVE('',#2694,#2693,#1530,.T.);
#3345=EDGE_CURVE('',#2687,#2694,#1531,.T.);
#3346=EDGE_CURVE('',#2695,#2694,#1532,.T.);
#3347=EDGE_CURVE('',#2680,#2695,#1533,.T.);
#3348=EDGE_CURVE('',#2688,#2695,#1534,.T.);
#4534=ORIENTED_EDGE('',*,*,#3319,.F.);
#4535=ORIENTED_EDGE('',*,*,#3320,.T.);
#4536=ORIENTED_EDGE('',*,*,#3321,.F.);
#4537=ORIENTED_EDGE('',*,*,#3320,.F.);
#4538=ORIENTED_EDGE('',*,*,#3322,.F.);
#4539=ORIENTED_EDGE('',*,*,#3323,.T.);
#4540=ORIENTED_EDGE('',*,*,#3324,.F.);
#4541=ORIENTED_EDGE('',*,*,#3323,.F.);
#4542=ORIENTED_EDGE('',*,*,#3325,.T.);
#4543=ORIENTED_EDGE('',*,*,#3326,.T.);
#4544=ORIENTED_EDGE('',*,*,#3327,.T.);
#4545=ORIENTED_EDGE('',*,*,#3328,.T.);
#4546=ORIENTED_EDGE('',*,*,#3329,.T.);
#4547=ORIENTED_EDGE('',*,*,#3330,.T.);
#4548=ORIENTED_EDGE('',*,*,#3331,.T.);
#4549=ORIENTED_EDGE('',*,*,#3332,.T.);
#4550=ORIENTED_EDGE('',*,*,#3333,.T.);
#4551=ORIENTED_EDGE('',*,*,#3334,.F.);
#4552=ORIENTED_EDGE('',*,*,#3335,.F.);
#4553=ORIENTED_EDGE('',*,*,#3326,.F.);
#4554=ORIENTED_EDGE('',*,*,#3335,.T.);
#4555=ORIENTED_EDGE('',*,*,#3336,.F.);
#4556=ORIENTED_EDGE('',*,*,#3337,.F.);
#4557=ORIENTED_EDGE('',*,*,#3327,.F.);
#4558=ORIENTED_EDGE('',*,*,#3322,.T.);
#4559=ORIENTED_EDGE('',*,*,#3337,.T.);
#4560=ORIENTED_EDGE('',*,*,#3338,.F.);
#4561=ORIENTED_EDGE('',*,*,#3339,.F.);
#4562=ORIENTED_EDGE('',*,*,#3328,.F.);
#4563=ORIENTED_EDGE('',*,*,#3339,.T.);
#4564=ORIENTED_EDGE('',*,*,#3340,.F.);
#4565=ORIENTED_EDGE('',*,*,#3341,.F.);
#4566=ORIENTED_EDGE('',*,*,#3329,.F.);
#4567=ORIENTED_EDGE('',*,*,#3321,.T.);
#4568=ORIENTED_EDGE('',*,*,#3324,.T.);
#4569=ORIENTED_EDGE('',*,*,#3341,.T.);
#4570=ORIENTED_EDGE('',*,*,#3342,.F.);
#4571=ORIENTED_EDGE('',*,*,#3343,.F.);
#4572=ORIENTED_EDGE('',*,*,#3330,.F.);
#4573=ORIENTED_EDGE('',*,*,#3343,.T.);
#4574=ORIENTED_EDGE('',*,*,#3344,.F.);
#4575=ORIENTED_EDGE('',*,*,#3345,.F.);
#4576=ORIENTED_EDGE('',*,*,#3331,.F.);
#4577=ORIENTED_EDGE('',*,*,#3319,.T.);
#4578=ORIENTED_EDGE('',*,*,#3345,.T.);
#4579=ORIENTED_EDGE('',*,*,#3346,.F.);
#4580=ORIENTED_EDGE('',*,*,#3347,.F.);
#4581=ORIENTED_EDGE('',*,*,#3332,.F.);
#4582=ORIENTED_EDGE('',*,*,#3347,.T.);
#4583=ORIENTED_EDGE('',*,*,#3348,.F.);
#4584=ORIENTED_EDGE('',*,*,#3333,.F.);
#4585=ORIENTED_EDGE('',*,*,#3325,.F.);
#4586=ORIENTED_EDGE('',*,*,#3348,.T.);
#4587=ORIENTED_EDGE('',*,*,#3346,.T.);
#4588=ORIENTED_EDGE('',*,*,#3344,.T.);
#4589=ORIENTED_EDGE('',*,*,#3342,.T.);
#4590=ORIENTED_EDGE('',*,*,#3340,.T.);
#4591=ORIENTED_EDGE('',*,*,#3338,.T.);
#4592=ORIENTED_EDGE('',*,*,#3336,.T.);
#4593=ORIENTED_EDGE('',*,*,#3334,.T.);
#5423=CYLINDRICAL_SURFACE('',#6310,3.00000000000001);
#5424=CYLINDRICAL_SURFACE('',#6313,3.);
#5703=ADVANCED_FACE('',(#640),#5423,.F.);
#5704=ADVANCED_FACE('',(#641),#5424,.F.);
#5705=ADVANCED_FACE('',(#642),#398,.T.);
#5706=ADVANCED_FACE('',(#643),#399,.T.);
#5707=ADVANCED_FACE('',(#644,#301),#400,.T.);
#5708=ADVANCED_FACE('',(#645),#401,.T.);
#5709=ADVANCED_FACE('',(#646,#302,#303),#402,.T.);
#5710=ADVANCED_FACE('',(#647),#403,.T.);
#5711=ADVANCED_FACE('',(#648,#304),#404,.T.);
#5712=ADVANCED_FACE('',(#649),#405,.T.);
#5713=ADVANCED_FACE('',(#650),#406,.T.);
#5714=ADVANCED_FACE('',(#651),#407,.T.);
#5884=CLOSED_SHELL('',(#5703,#5704,#5705,#5706,#5707,#5708,#5709,#5710,
#5711,#5712,#5713,#5714));
#6309=AXIS2_PLACEMENT_3D('',#9286,#7515,#7516);
#6310=AXIS2_PLACEMENT_3D('',#9287,#7517,#7518);
#6311=AXIS2_PLACEMENT_3D('',#9289,#7519,#7520);
#6312=AXIS2_PLACEMENT_3D('',#9292,#7522,#7523);
#6313=AXIS2_PLACEMENT_3D('',#9293,#7524,#7525);
#6314=AXIS2_PLACEMENT_3D('',#9295,#7526,#7527);
#6315=AXIS2_PLACEMENT_3D('',#9298,#7529,#7530);
#6316=AXIS2_PLACEMENT_3D('',#9299,#7531,#7532);
#6317=AXIS2_PLACEMENT_3D('',#9316,#7541,#7542);
#6318=AXIS2_PLACEMENT_3D('',#9322,#7546,#7547);
#6319=AXIS2_PLACEMENT_3D('',#9326,#7550,#7551);
#6320=AXIS2_PLACEMENT_3D('',#9330,#7554,#7555);
#6321=AXIS2_PLACEMENT_3D('',#9334,#7558,#7559);
#6322=AXIS2_PLACEMENT_3D('',#9338,#7562,#7563);
#6323=AXIS2_PLACEMENT_3D('',#9342,#7566,#7567);
#6324=AXIS2_PLACEMENT_3D('',#9346,#7570,#7571);
#6325=AXIS2_PLACEMENT_3D('',#9348,#7573,#7574);
#7515=DIRECTION('axis',(0.,0.,1.));
#7516=DIRECTION('refdir',(1.,0.,0.));
#7517=DIRECTION('center_axis',(0.,1.,0.));
#7518=DIRECTION('ref_axis',(1.,0.,0.));
#7519=DIRECTION('center_axis',(0.,1.,0.));
#7520=DIRECTION('ref_axis',(1.,0.,0.));
#7521=DIRECTION('',(0.,1.,0.));
#7522=DIRECTION('center_axis',(0.,-1.,0.));
#7523=DIRECTION('ref_axis',(1.,0.,0.));
#7524=DIRECTION('center_axis',(0.,1.,0.));
#7525=DIRECTION('ref_axis',(1.,0.,0.));
#7526=DIRECTION('center_axis',(0.,1.,0.));
#7527=DIRECTION('ref_axis',(1.,0.,0.));
#7528=DIRECTION('',(0.,1.,0.));
#7529=DIRECTION('center_axis',(0.,-1.,0.));
#7530=DIRECTION('ref_axis',(1.,0.,0.));
#7531=DIRECTION('center_axis',(0.,0.,-1.));
#7532=DIRECTION('ref_axis',(-1.,0.,0.));
#7533=DIRECTION('',(-1.,0.,0.));
#7534=DIRECTION('',(-0.268631512041369,0.963243017487471,0.));
#7535=DIRECTION('',(-1.,0.,0.));
#7536=DIRECTION('',(0.,1.,0.));
#7537=DIRECTION('',(1.,0.,0.));
#7538=DIRECTION('',(0.,-1.,0.));
#7539=DIRECTION('',(-1.,0.,0.));
#7540=DIRECTION('',(-0.268631512041369,-0.963243017487471,0.));
#7541=DIRECTION('center_axis',(-0.963243017487471,-0.268631512041369,0.));
#7542=DIRECTION('ref_axis',(0.268631512041369,-0.963243017487471,0.));
#7543=DIRECTION('',(0.,0.,1.));
#7544=DIRECTION('',(0.268631512041369,-0.963243017487471,0.));
#7545=DIRECTION('',(0.,0.,1.));
#7546=DIRECTION('center_axis',(0.,-1.,0.));
#7547=DIRECTION('ref_axis',(1.,0.,0.));
#7548=DIRECTION('',(1.,0.,0.));
#7549=DIRECTION('',(0.,0.,1.));
#7550=DIRECTION('center_axis',(-1.,0.,0.));
#7551=DIRECTION('ref_axis',(0.,-1.,0.));
#7552=DIRECTION('',(0.,-1.,0.));
#7553=DIRECTION('',(0.,0.,1.));
#7554=DIRECTION('center_axis',(0.,1.,0.));
#7555=DIRECTION('ref_axis',(-1.,0.,0.));
#7556=DIRECTION('',(-1.,0.,0.));
#7557=DIRECTION('',(0.,0.,1.));
#7558=DIRECTION('center_axis',(1.,0.,0.));
#7559=DIRECTION('ref_axis',(0.,1.,0.));
#7560=DIRECTION('',(0.,1.,0.));
#7561=DIRECTION('',(0.,0.,1.));
#7562=DIRECTION('center_axis',(0.,-1.,0.));
#7563=DIRECTION('ref_axis',(1.,0.,0.));
#7564=DIRECTION('',(1.,0.,0.));
#7565=DIRECTION('',(0.,0.,1.));
#7566=DIRECTION('center_axis',(0.963243017487471,-0.268631512041369,0.));
#7567=DIRECTION('ref_axis',(0.268631512041369,0.963243017487471,0.));
#7568=DIRECTION('',(0.268631512041369,0.963243017487471,0.));
#7569=DIRECTION('',(0.,0.,1.));
#7570=DIRECTION('center_axis',(0.,-1.,0.));
#7571=DIRECTION('ref_axis',(1.,0.,0.));
#7572=DIRECTION('',(1.,0.,0.));
#7573=DIRECTION('center_axis',(0.,0.,1.));
#7574=DIRECTION('ref_axis',(1.,0.,0.));
#9286=CARTESIAN_POINT('',(0.,0.,0.));
#9287=CARTESIAN_POINT('Origin',(21.2760503877808,-85.,85.));
#9288=CARTESIAN_POINT('',(18.2760503877808,-85.,85.));
#9289=CARTESIAN_POINT('Origin',(21.2760503877808,-85.,85.));
#9290=CARTESIAN_POINT('',(18.2760503877808,-82.,85.));
#9291=CARTESIAN_POINT('',(18.2760503877808,-85.,85.));
#9292=CARTESIAN_POINT('Origin',(21.2760503877808,-82.,85.));
#9293=CARTESIAN_POINT('Origin',(-20.7760503877808,-85.,85.));
#9294=CARTESIAN_POINT('',(-23.7760503877808,-85.,85.));
#9295=CARTESIAN_POINT('Origin',(-20.7760503877808,-85.,85.));
#9296=CARTESIAN_POINT('',(-23.7760503877808,-82.,85.));
#9297=CARTESIAN_POINT('',(-23.7760503877808,-85.,85.));
#9298=CARTESIAN_POINT('Origin',(-20.7760503877808,-82.,85.));
#9299=CARTESIAN_POINT('Origin',(0.249999999999999,-96.1435033236749,79.));
#9300=CARTESIAN_POINT('',(2.24999999999999,-110.28700664735,79.));
#9301=CARTESIAN_POINT('',(-1.75000000000001,-110.28700664735,79.));
#9302=CARTESIAN_POINT('',(0.249999999999995,-110.28700664735,79.));
#9303=CARTESIAN_POINT('',(-8.80210077556162,-85.,79.));
#9304=CARTESIAN_POINT('',(-1.75000000000001,-110.28700664735,79.));
#9305=CARTESIAN_POINT('',(-32.75,-85.,79.));
#9306=CARTESIAN_POINT('',(-32.75,-85.,79.));
#9307=CARTESIAN_POINT('',(-32.75,-82.,79.));
#9308=CARTESIAN_POINT('',(-32.75,-79.,79.));
#9309=CARTESIAN_POINT('',(33.25,-82.,79.));
#9310=CARTESIAN_POINT('',(-44.5857864376269,-82.,79.));
#9311=CARTESIAN_POINT('',(33.25,-85.,79.));
#9312=CARTESIAN_POINT('',(33.25,-85.,79.));
#9313=CARTESIAN_POINT('',(9.30210077556161,-85.,79.));
#9314=CARTESIAN_POINT('',(-32.75,-85.,79.));
#9315=CARTESIAN_POINT('',(2.24999999999999,-110.28700664735,79.));
#9316=CARTESIAN_POINT('Origin',(-8.80210077556162,-85.,85.));
#9317=CARTESIAN_POINT('',(-1.75000000000001,-110.28700664735,91.));
#9318=CARTESIAN_POINT('',(-1.75000000000001,-110.28700664735,85.));
#9319=CARTESIAN_POINT('',(-8.80210077556162,-85.,91.));
#9320=CARTESIAN_POINT('',(-1.75000000000001,-110.28700664735,91.));
#9321=CARTESIAN_POINT('',(-8.80210077556162,-85.,85.));
#9322=CARTESIAN_POINT('Origin',(-32.75,-85.,85.));
#9323=CARTESIAN_POINT('',(-32.75,-85.,91.));
#9324=CARTESIAN_POINT('',(-32.75,-85.,91.));
#9325=CARTESIAN_POINT('',(-32.75,-85.,85.));
#9326=CARTESIAN_POINT('Origin',(-32.75,-82.,85.));
#9327=CARTESIAN_POINT('',(-32.75,-82.,91.));
#9328=CARTESIAN_POINT('',(-32.75,-79.,91.));
#9329=CARTESIAN_POINT('',(-32.75,-82.,85.));
#9330=CARTESIAN_POINT('Origin',(33.25,-82.,85.));
#9331=CARTESIAN_POINT('',(33.25,-82.,91.));
#9332=CARTESIAN_POINT('',(-44.5857864376269,-82.,91.));
#9333=CARTESIAN_POINT('',(33.25,-82.,85.));
#9334=CARTESIAN_POINT('Origin',(33.25,-85.,85.));
#9335=CARTESIAN_POINT('',(33.25,-85.,91.));
#9336=CARTESIAN_POINT('',(33.25,-85.,91.));
#9337=CARTESIAN_POINT('',(33.25,-85.,85.));
#9338=CARTESIAN_POINT('Origin',(9.30210077556162,-85.,85.));
#9339=CARTESIAN_POINT('',(9.30210077556161,-85.,91.));
#9340=CARTESIAN_POINT('',(-32.75,-85.,91.));
#9341=CARTESIAN_POINT('',(9.30210077556161,-85.,85.));
#9342=CARTESIAN_POINT('Origin',(2.24999999999999,-110.28700664735,85.));
#9343=CARTESIAN_POINT('',(2.24999999999999,-110.28700664735,91.));
#9344=CARTESIAN_POINT('',(2.24999999999999,-110.28700664735,91.));
#9345=CARTESIAN_POINT('',(2.24999999999999,-110.28700664735,85.));
#9346=CARTESIAN_POINT('Origin',(-1.75000000000001,-110.28700664735,85.));
#9347=CARTESIAN_POINT('',(0.249999999999995,-110.28700664735,91.));
#9348=CARTESIAN_POINT('Origin',(0.249999999999999,-96.1435033236749,91.));
#10114=UNCERTAINTY_MEASURE_WITH_UNIT(LENGTH_MEASURE(0.01),#10132,
'DISTANCE_ACCURACY_VALUE',
'Maximum model space distance between geometric entities at asserted c
onnectivities');
#10119=UNCERTAINTY_MEASURE_WITH_UNIT(LENGTH_MEASURE(0.01),#10132,
'DISTANCE_ACCURACY_VALUE',
'Maximum model space distance between geometric entities at asserted c
onnectivities');
#10126=(
GEOMETRIC_REPRESENTATION_CONTEXT(3)
GLOBAL_UNCERTAINTY_ASSIGNED_CONTEXT((#10114))
GLOBAL_UNIT_ASSIGNED_CONTEXT((#10132,#10134,#10135))
REPRESENTATION_CONTEXT('','3D')
);
#10131=(
GEOMETRIC_REPRESENTATION_CONTEXT(3)
GLOBAL_UNCERTAINTY_ASSIGNED_CONTEXT((#10119))
GLOBAL_UNIT_ASSIGNED_CONTEXT((#10132,#10134,#10135))
REPRESENTATION_CONTEXT('','3D')
);
#10132=(
LENGTH_UNIT()
NAMED_UNIT(*)
SI_UNIT(.MILLI.,.METRE.)
);
#10134=(
NAMED_UNIT(*)
PLANE_ANGLE_UNIT()
SI_UNIT($,.RADIAN.)
);
#10135=(
NAMED_UNIT(*)
SI_UNIT($,.STERADIAN.)
SOLID_ANGLE_UNIT()
);
#10142=SHAPE_DEFINITION_REPRESENTATION(#10153,#10174);
#10153=PRODUCT_DEFINITION_SHAPE('',$,#10186);
#10174=SHAPE_REPRESENTATION('',(#6309),#10126);
#10179=PRODUCT_DEFINITION_CONTEXT('part definition',#10214,'design');
#10186=PRODUCT_DEFINITION('Front_Mount','Front_Mount',#10197,#10179);
#10197=PRODUCT_DEFINITION_FORMATION('',$,#10222);
#10214=APPLICATION_CONTEXT(
'Core Data for Automotive Mechanical Design Process');
#10215=PRODUCT_CONTEXT('part definition',#10214,'mechanical');
#10222=PRODUCT('Front_Mount','Front_Mount',$,(#10215));
#10255=COLOUR_RGB('Sky Blue',0.24,0.69,0.87);
#10256=FILL_AREA_STYLE_COLOUR('',#10255);
#10257=FILL_AREA_STYLE('',(#10256));
#10258=SURFACE_STYLE_FILL_AREA(#10257);
#10259=SURFACE_SIDE_STYLE('',(#10258));
#10260=SURFACE_STYLE_USAGE(.BOTH.,#10259);
#10261=PRESENTATION_STYLE_ASSIGNMENT((#10260));
ENDSEC;
END-ISO-10303-21;
